ISO-10303-21;
HEADER;
FILE_DESCRIPTION((''),'2;1');
FILE_NAME('Shaft Spring Washer.step','2026-10-06T07:01:46+05:00',(''),(''),'','','');
FILE_SCHEMA (('AUTOMOTIVE_DESIGN { 1 0 10303 214 3 1 1 }'));
ENDSEC;
DATA;
#10=MECHANICAL_DESIGN_GEOMETRIC_PRESENTATION_REPRESENTATION('',(#148),#11396);
#118=SHAPE_REPRESENTATION_RELATIONSHIP('SRR','None',#11465,#133) ;
#133=ADVANCED_BREP_SHAPE_REPRESENTATION('',(#163),#11391) ;
#148=STYLED_ITEM('',(#11549),#163) ;
#163=MANIFOLD_SOLID_BREP('Shaft Spring Washer',#5579) ;
#370=FACE_BOUND('',#1180,.T.) ;
#371=FACE_BOUND('',#1183,.T.) ;
#490=PLANE('',#6324) ;
#491=PLANE('',#6328) ;
#809=FACE_OUTER_BOUND('',#1178,.T.) ;
#810=FACE_OUTER_BOUND('',#1179,.T.) ;
#811=FACE_OUTER_BOUND('',#1181,.T.) ;
#812=FACE_OUTER_BOUND('',#1182,.T.) ;
#1178=EDGE_LOOP('',(#4942,#4943,#4944,#4945)) ;
#1179=EDGE_LOOP('',(#4946)) ;
#1180=EDGE_LOOP('',(#4947)) ;
#1181=EDGE_LOOP('',(#4948,#4949,#4950,#4951)) ;
#1182=EDGE_LOOP('',(#4952)) ;
#1183=EDGE_LOOP('',(#4953)) ;
#1563=LINE('',#11182,#1946) ;
#1564=LINE('',#11190,#1947) ;
#1946=VECTOR('',#7903,3.985) ;
#1947=VECTOR('',#7914,5.4) ;
#2235=CIRCLE('',#6322,3.985) ;
#2236=CIRCLE('',#6323,3.985) ;
#2237=CIRCLE('',#6325,5.4) ;
#2238=CIRCLE('',#6327,5.4) ;
#2696=VERTEX_POINT('',#11179) ;
#2697=VERTEX_POINT('',#11181) ;
#2698=VERTEX_POINT('',#11185) ;
#2699=VERTEX_POINT('',#11188) ;
#3453=EDGE_CURVE('',#2696,#2696,#2235,.T.) ;
#3454=EDGE_CURVE('',#2696,#2697,#1563,.T.) ;
#3455=EDGE_CURVE('',#2697,#2697,#2236,.T.) ;
#3456=EDGE_CURVE('',#2698,#2698,#2237,.T.) ;
#3457=EDGE_CURVE('',#2699,#2699,#2238,.T.) ;
#3458=EDGE_CURVE('',#2699,#2698,#1564,.T.) ;
#4942=ORIENTED_EDGE('',*,*,#3453,.T.) ;
#4943=ORIENTED_EDGE('',*,*,#3454,.T.) ;
#4944=ORIENTED_EDGE('',*,*,#3455,.F.) ;
#4945=ORIENTED_EDGE('',*,*,#3454,.F.) ;
#4946=ORIENTED_EDGE('',*,*,#3456,.F.) ;
#4947=ORIENTED_EDGE('',*,*,#3455,.T.) ;
#4948=ORIENTED_EDGE('',*,*,#3457,.F.) ;
#4949=ORIENTED_EDGE('',*,*,#3458,.T.) ;
#4950=ORIENTED_EDGE('',*,*,#3456,.T.) ;
#4951=ORIENTED_EDGE('',*,*,#3458,.F.) ;
#4952=ORIENTED_EDGE('',*,*,#3457,.T.) ;
#4953=ORIENTED_EDGE('',*,*,#3453,.F.) ;
#5216=CYLINDRICAL_SURFACE('',#6321,3.985) ;
#5217=CYLINDRICAL_SURFACE('',#6326,5.4) ;
#5534=ADVANCED_FACE('',(#809),#5216,.F.) ;
#5535=ADVANCED_FACE('',(#810,#370),#490,.T.) ;
#5536=ADVANCED_FACE('',(#811),#5217,.T.) ;
#5537=ADVANCED_FACE('',(#812,#371),#491,.T.) ;
#5579=CLOSED_SHELL('',(#5534,#5535,#5536,#5537)) ;
#6320=AXIS2_PLACEMENT_3D('',#11177,#7897,#7898) ;
#6321=AXIS2_PLACEMENT_3D('',#11178,#7899,#7900) ;
#6322=AXIS2_PLACEMENT_3D('',#11180,#7901,#7902) ;
#6323=AXIS2_PLACEMENT_3D('',#11183,#7904,#7905) ;
#6324=AXIS2_PLACEMENT_3D('',#11184,#7906,#7907) ;
#6325=AXIS2_PLACEMENT_3D('',#11186,#7908,#7909) ;
#6326=AXIS2_PLACEMENT_3D('',#11187,#7910,#7911) ;
#6327=AXIS2_PLACEMENT_3D('',#11189,#7912,#7913) ;
#6328=AXIS2_PLACEMENT_3D('',#11191,#7915,#7916) ;
#7897=DIRECTION('axis',(0.,0.,1.)) ;
#7898=DIRECTION('refdir',(1.,0.,0.)) ;
#7899=DIRECTION('center_axis',(1.,0.,0.)) ;
#7900=DIRECTION('ref_axis',(0.,1.,0.)) ;
#7901=DIRECTION('center_axis',(1.,0.,0.)) ;
#7902=DIRECTION('ref_axis',(0.,0.,-1.)) ;
#7903=DIRECTION('',(-1.,0.,0.)) ;
#7904=DIRECTION('center_axis',(1.,0.,0.)) ;
#7905=DIRECTION('ref_axis',(0.,0.,-1.)) ;
#7906=DIRECTION('center_axis',(-1.,0.,0.)) ;
#7907=DIRECTION('ref_axis',(0.,0.,1.)) ;
#7908=DIRECTION('center_axis',(1.,0.,0.)) ;
#7909=DIRECTION('ref_axis',(0.,0.,-1.)) ;
#7910=DIRECTION('center_axis',(1.,0.,0.)) ;
#7911=DIRECTION('ref_axis',(0.,1.,0.)) ;
#7912=DIRECTION('center_axis',(1.,0.,0.)) ;
#7913=DIRECTION('ref_axis',(0.,0.,-1.)) ;
#7914=DIRECTION('',(-1.,0.,0.)) ;
#7915=DIRECTION('center_axis',(1.,0.,0.)) ;
#7916=DIRECTION('ref_axis',(0.,0.,-1.)) ;
#11177=CARTESIAN_POINT('',(0.,0.,0.)) ;
#11178=CARTESIAN_POINT('Origin',(-25.6575,17.565,27.14)) ;
#11179=CARTESIAN_POINT('',(-25.34,13.58,27.14)) ;
#11180=CARTESIAN_POINT('Origin',(-25.34,17.565,27.14)) ;
#11181=CARTESIAN_POINT('',(-25.975,13.58,27.14)) ;
#11182=CARTESIAN_POINT('',(-25.6575,13.58,27.14)) ;
#11183=CARTESIAN_POINT('Origin',(-25.975,17.565,27.14)) ;
#11184=CARTESIAN_POINT('Origin',(-25.975,22.965,27.14)) ;
#11185=CARTESIAN_POINT('',(-25.975,12.165,27.14)) ;
#11186=CARTESIAN_POINT('Origin',(-25.975,17.565,27.14)) ;
#11187=CARTESIAN_POINT('Origin',(-25.6575,17.565,27.14)) ;
#11188=CARTESIAN_POINT('',(-25.34,12.165,27.14)) ;
#11189=CARTESIAN_POINT('Origin',(-25.34,17.565,27.14)) ;
#11190=CARTESIAN_POINT('',(-25.6575,12.165,27.14)) ;
#11191=CARTESIAN_POINT('Origin',(-25.34,21.55,27.14)) ;
#11374=UNCERTAINTY_MEASURE_WITH_UNIT(LENGTH_MEASURE(0.01),#11397,
'DISTANCE_ACCURACY_VALUE',
'Maximum model space distance between geometric entities at asserted c
onnectivities') ;
#11379=UNCERTAINTY_MEASURE_WITH_UNIT(LENGTH_MEASURE(0.01),#11397,
'DISTANCE_ACCURACY_VALUE',
'Maximum model space distance between geometric entities at asserted c
onnectivities') ;
#11391=(
GEOMETRIC_REPRESENTATION_CONTEXT(3)
GLOBAL_UNCERTAINTY_ASSIGNED_CONTEXT((#11374))
GLOBAL_UNIT_ASSIGNED_CONTEXT((#11397,#11399,#11400))
REPRESENTATION_CONTEXT('','3D')
) ;
#11396=(
GEOMETRIC_REPRESENTATION_CONTEXT(3)
GLOBAL_UNCERTAINTY_ASSIGNED_CONTEXT((#11379))
GLOBAL_UNIT_ASSIGNED_CONTEXT((#11397,#11399,#11400))
REPRESENTATION_CONTEXT('','3D')
) ;
#11397=(
LENGTH_UNIT()
NAMED_UNIT(*)
SI_UNIT(.MILLI.,.METRE.)
) ;
#11399=(
NAMED_UNIT(*)
PLANE_ANGLE_UNIT()
SI_UNIT($,.RADIAN.)
) ;
#11400=(
NAMED_UNIT(*)
SI_UNIT($,.STERADIAN.)
SOLID_ANGLE_UNIT()
) ;
#11412=SHAPE_DEFINITION_REPRESENTATION(#11428,#11465) ;
#11428=PRODUCT_DEFINITION_SHAPE('',$,#11482) ;
#11465=SHAPE_REPRESENTATION('',(#6320),#11391) ;
#11470=PRODUCT_DEFINITION_CONTEXT('part definition',#11520,'design') ;
#11482=PRODUCT_DEFINITION('Shaft Spring Washer',
'Shaft Spring Washer',#11498,#11470) ;
#11498=PRODUCT_DEFINITION_FORMATION('',$,#11533) ;
#11520=APPLICATION_CONTEXT(
'Core Data for Automotive Mechanical Design Process') ;
#11521=PRODUCT_CONTEXT('part definition',#11520,'mechanical') ;
#11533=PRODUCT('Shaft Spring Washer','Shaft Spring Washer',$,(#11521)) ;
#11549=PRESENTATION_STYLE_ASSIGNMENT((#11565)) ;
#11565=SURFACE_STYLE_USAGE(.BOTH.,#11581) ;
#11581=SURFACE_SIDE_STYLE('',(#11597)) ;
#11597=SURFACE_STYLE_FILL_AREA(#11613) ;
#11613=FILL_AREA_STYLE('MAS-252 Metallic - Shaft Spring Washer',(#11629)) ;
#11629=FILL_AREA_STYLE_COLOUR('MAS-252 Metallic - Shaft Spring Washer',
#11645) ;
#11645=COLOUR_RGB('MAS-252 Metallic - Shaft Spring Washer', 0.72549020, 0.75294118, 0.79215686) ;
ENDSEC;
END-ISO-10303-21;
